ISO-10303-21;
HEADER;
/* Generated by software containing ST-Developer
 * from STEP Tools, Inc. (www.steptools.com) 
 */

FILE_DESCRIPTION(
/* description */ ('Bin tilter linkage'),
/* implementation_level */ '2;1');

FILE_NAME(
/* name */ 'M4x10 Cap Screw.step',
/* time_stamp */ '2026-10-28T03:26:24-07:00',
/* author */ (''),
/* organization */ (''),
/* preprocessor_version */ 'ST-DEVELOPER v20.2',
/* originating_system */ 'Autodesk Translation Framework v15.17.0.0',
/* authorisation */ '');

FILE_SCHEMA (('AUTOMOTIVE_DESIGN { 1 0 10303 214 3 1 1 }'));
ENDSEC;

DATA;
#10=MECHANICAL_DESIGN_GEOMETRIC_PRESENTATION_REPRESENTATION('',(#969),#23728);
#631=ORIENTED_CLOSED_SHELL('',*,#12501,.F.);
#644=CONICAL_SURFACE('',#15382,0.325,0.785398163397448);
#645=CONICAL_SURFACE('',#15386,0.335,0.785398163397448);
#646=CONICAL_SURFACE('',#15390,0.21,0.463647609000806);
#649=BREP_WITH_VOIDS('Body1',#12502,(#631));
#749=SHAPE_REPRESENTATION_RELATIONSHIP('SRR','None',#24219,#855);
#855=ADVANCED_BREP_SHAPE_REPRESENTATION('',(#649),#23719);
#969=STYLED_ITEM('',(#24772),#649);
#1481=FACE_BOUND('',#3810,.T.);
#1865=PLANE('',#15370);
#1866=PLANE('',#15371);
#1867=PLANE('',#15372);
#1868=PLANE('',#15373);
#1869=PLANE('',#15374);
#1870=PLANE('',#15375);
#1871=PLANE('',#15376);
#1872=PLANE('',#15377);
#1873=PLANE('',#15378);
#1874=PLANE('',#15380);
#1875=PLANE('',#15388);
#2625=FACE_OUTER_BOUND('',#3796,.T.);
#2626=FACE_OUTER_BOUND('',#3797,.T.);
#2627=FACE_OUTER_BOUND('',#3798,.T.);
#2628=FACE_OUTER_BOUND('',#3799,.T.);
#2629=FACE_OUTER_BOUND('',#3800,.T.);
#2630=FACE_OUTER_BOUND('',#3801,.T.);
#2631=FACE_OUTER_BOUND('',#3802,.T.);
#2632=FACE_OUTER_BOUND('',#3803,.T.);
#2633=FACE_OUTER_BOUND('',#3804,.T.);
#2634=FACE_OUTER_BOUND('',#3805,.T.);
#2635=FACE_OUTER_BOUND('',#3806,.T.);
#2636=FACE_OUTER_BOUND('',#3807,.T.);
#2637=FACE_OUTER_BOUND('',#3808,.T.);
#2638=FACE_OUTER_BOUND('',#3809,.T.);
#2639=FACE_OUTER_BOUND('',#3811,.T.);
#2640=FACE_OUTER_BOUND('',#3812,.T.);
#3796=EDGE_LOOP('',(#11123,#11124,#11125,#11126));
#3797=EDGE_LOOP('',(#11127,#11128,#11129,#11130));
#3798=EDGE_LOOP('',(#11131,#11132,#11133,#11134));
#3799=EDGE_LOOP('',(#11135,#11136,#11137,#11138));
#3800=EDGE_LOOP('',(#11139,#11140,#11141,#11142));
#3801=EDGE_LOOP('',(#11143,#11144,#11145,#11146));
#3802=EDGE_LOOP('',(#11147,#11148,#11149,#11150,#11151,#11152));
#3803=EDGE_LOOP('',(#11153,#11154,#11155,#11156,#11157,#11158));
#3804=EDGE_LOOP('',(#11159));
#3805=EDGE_LOOP('',(#11160));
#3806=EDGE_LOOP('',(#11161,#11162,#11163,#11164));
#3807=EDGE_LOOP('',(#11165,#11166,#11167,#11168));
#3808=EDGE_LOOP('',(#11169,#11170,#11171,#11172));
#3809=EDGE_LOOP('',(#11173));
#3810=EDGE_LOOP('',(#11174));
#3811=EDGE_LOOP('',(#11175,#11176,#11177,#11178));
#3812=EDGE_LOOP('',(#11179,#11180,#11181,#11182));
#4483=LINE('',#23306,#5158);
#4484=LINE('',#23308,#5159);
#4485=LINE('',#23310,#5160);
#4486=LINE('',#23311,#5161);
#4487=LINE('',#23314,#5162);
#4488=LINE('',#23316,#5163);
#4489=LINE('',#23317,#5164);
#4490=LINE('',#23320,#5165);
#4491=LINE('',#23322,#5166);
#4492=LINE('',#23323,#5167);
#4493=LINE('',#23326,#5168);
#4494=LINE('',#23328,#5169);
#4495=LINE('',#23329,#5170);
#4496=LINE('',#23332,#5171);
#4497=LINE('',#23334,#5172);
#4498=LINE('',#23335,#5173);
#4499=LINE('',#23337,#5174);
#4500=LINE('',#23338,#5175);
#4501=LINE('',#23350,#5176);
#4502=LINE('',#23354,#5177);
#4503=LINE('',#23358,#5178);
#4504=LINE('',#23365,#5179);
#4505=LINE('',#23367,#5180);
#5158=VECTOR('',#19498,1.);
#5159=VECTOR('',#19499,1.);
#5160=VECTOR('',#19500,1.);
#5161=VECTOR('',#19501,1.);
#5162=VECTOR('',#19504,1.);
#5163=VECTOR('',#19505,1.);
#5164=VECTOR('',#19506,1.);
#5165=VECTOR('',#19509,1.);
#5166=VECTOR('',#19510,1.);
#5167=VECTOR('',#19511,1.);
#5168=VECTOR('',#19514,1.);
#5169=VECTOR('',#19515,1.);
#5170=VECTOR('',#19516,1.);
#5171=VECTOR('',#19519,1.);
#5172=VECTOR('',#19520,1.);
#5173=VECTOR('',#19521,1.);
#5174=VECTOR('',#19524,1.);
#5175=VECTOR('',#19525,1.);
#5176=VECTOR('',#19542,0.325);
#5177=VECTOR('',#19547,0.35);
#5178=VECTOR('',#19552,0.335);
#5179=VECTOR('',#19561,0.21);
#5180=VECTOR('',#19564,0.2);
#5926=CIRCLE('',#15379,0.1954);
#5927=CIRCLE('',#15381,0.3);
#5928=CIRCLE('',#15383,0.35);
#5929=CIRCLE('',#15385,0.35);
#5930=CIRCLE('',#15387,0.32);
#5931=CIRCLE('',#15389,0.22);
#5932=CIRCLE('',#15391,0.1954);
#6879=VERTEX_POINT('',#23304);
#6880=VERTEX_POINT('',#23305);
#6881=VERTEX_POINT('',#23307);
#6882=VERTEX_POINT('',#23309);
#6883=VERTEX_POINT('',#23313);
#6884=VERTEX_POINT('',#23315);
#6885=VERTEX_POINT('',#23319);
#6886=VERTEX_POINT('',#23321);
#6887=VERTEX_POINT('',#23325);
#6888=VERTEX_POINT('',#23327);
#6889=VERTEX_POINT('',#23331);
#6890=VERTEX_POINT('',#23333);
#6891=VERTEX_POINT('',#23342);
#6892=VERTEX_POINT('',#23345);
#6893=VERTEX_POINT('',#23348);
#6894=VERTEX_POINT('',#23352);
#6895=VERTEX_POINT('',#23356);
#6896=VERTEX_POINT('',#23360);
#6897=VERTEX_POINT('',#23363);
#8301=EDGE_CURVE('',#6879,#6880,#4483,.T.);
#8302=EDGE_CURVE('',#6880,#6881,#4484,.T.);
#8303=EDGE_CURVE('',#6881,#6882,#4485,.T.);
#8304=EDGE_CURVE('',#6879,#6882,#4486,.T.);
#8305=EDGE_CURVE('',#6880,#6883,#4487,.T.);
#8306=EDGE_CURVE('',#6883,#6884,#4488,.T.);
#8307=EDGE_CURVE('',#6884,#6881,#4489,.T.);
#8308=EDGE_CURVE('',#6883,#6885,#4490,.T.);
#8309=EDGE_CURVE('',#6885,#6886,#4491,.T.);
#8310=EDGE_CURVE('',#6886,#6884,#4492,.T.);
#8311=EDGE_CURVE('',#6885,#6887,#4493,.T.);
#8312=EDGE_CURVE('',#6887,#6888,#4494,.T.);
#8313=EDGE_CURVE('',#6888,#6886,#4495,.T.);
#8314=EDGE_CURVE('',#6887,#6889,#4496,.T.);
#8315=EDGE_CURVE('',#6889,#6890,#4497,.T.);
#8316=EDGE_CURVE('',#6890,#6888,#4498,.T.);
#8317=EDGE_CURVE('',#6889,#6879,#4499,.T.);
#8318=EDGE_CURVE('',#6882,#6890,#4500,.T.);
#8319=EDGE_CURVE('',#6891,#6891,#5926,.T.);
#8320=EDGE_CURVE('',#6892,#6892,#5927,.T.);
#8321=EDGE_CURVE('',#6893,#6893,#5928,.T.);
#8322=EDGE_CURVE('',#6893,#6892,#4501,.T.);
#8323=EDGE_CURVE('',#6894,#6894,#5929,.T.);
#8324=EDGE_CURVE('',#6894,#6893,#4502,.T.);
#8325=EDGE_CURVE('',#6895,#6895,#5930,.T.);
#8326=EDGE_CURVE('',#6895,#6894,#4503,.T.);
#8327=EDGE_CURVE('',#6896,#6896,#5931,.T.);
#8328=EDGE_CURVE('',#6897,#6897,#5932,.F.);
#8329=EDGE_CURVE('',#6897,#6896,#4504,.T.);
#8330=EDGE_CURVE('',#6891,#6897,#4505,.T.);
#11123=ORIENTED_EDGE('',*,*,#8301,.T.);
#11124=ORIENTED_EDGE('',*,*,#8302,.T.);
#11125=ORIENTED_EDGE('',*,*,#8303,.T.);
#11126=ORIENTED_EDGE('',*,*,#8304,.F.);
#11127=ORIENTED_EDGE('',*,*,#8305,.T.);
#11128=ORIENTED_EDGE('',*,*,#8306,.T.);
#11129=ORIENTED_EDGE('',*,*,#8307,.T.);
#11130=ORIENTED_EDGE('',*,*,#8302,.F.);
#11131=ORIENTED_EDGE('',*,*,#8308,.T.);
#11132=ORIENTED_EDGE('',*,*,#8309,.T.);
#11133=ORIENTED_EDGE('',*,*,#8310,.T.);
#11134=ORIENTED_EDGE('',*,*,#8306,.F.);
#11135=ORIENTED_EDGE('',*,*,#8311,.T.);
#11136=ORIENTED_EDGE('',*,*,#8312,.T.);
#11137=ORIENTED_EDGE('',*,*,#8313,.T.);
#11138=ORIENTED_EDGE('',*,*,#8309,.F.);
#11139=ORIENTED_EDGE('',*,*,#8314,.T.);
#11140=ORIENTED_EDGE('',*,*,#8315,.T.);
#11141=ORIENTED_EDGE('',*,*,#8316,.T.);
#11142=ORIENTED_EDGE('',*,*,#8312,.F.);
#11143=ORIENTED_EDGE('',*,*,#8317,.T.);
#11144=ORIENTED_EDGE('',*,*,#8304,.T.);
#11145=ORIENTED_EDGE('',*,*,#8318,.T.);
#11146=ORIENTED_EDGE('',*,*,#8315,.F.);
#11147=ORIENTED_EDGE('',*,*,#8317,.F.);
#11148=ORIENTED_EDGE('',*,*,#8314,.F.);
#11149=ORIENTED_EDGE('',*,*,#8311,.F.);
#11150=ORIENTED_EDGE('',*,*,#8308,.F.);
#11151=ORIENTED_EDGE('',*,*,#8305,.F.);
#11152=ORIENTED_EDGE('',*,*,#8301,.F.);
#11153=ORIENTED_EDGE('',*,*,#8318,.F.);
#11154=ORIENTED_EDGE('',*,*,#8303,.F.);
#11155=ORIENTED_EDGE('',*,*,#8307,.F.);
#11156=ORIENTED_EDGE('',*,*,#8310,.F.);
#11157=ORIENTED_EDGE('',*,*,#8313,.F.);
#11158=ORIENTED_EDGE('',*,*,#8316,.F.);
#11159=ORIENTED_EDGE('',*,*,#8319,.F.);
#11160=ORIENTED_EDGE('',*,*,#8320,.F.);
#11161=ORIENTED_EDGE('',*,*,#8321,.F.);
#11162=ORIENTED_EDGE('',*,*,#8322,.T.);
#11163=ORIENTED_EDGE('',*,*,#8320,.T.);
#11164=ORIENTED_EDGE('',*,*,#8322,.F.);
#11165=ORIENTED_EDGE('',*,*,#8323,.F.);
#11166=ORIENTED_EDGE('',*,*,#8324,.T.);
#11167=ORIENTED_EDGE('',*,*,#8321,.T.);
#11168=ORIENTED_EDGE('',*,*,#8324,.F.);
#11169=ORIENTED_EDGE('',*,*,#8325,.F.);
#11170=ORIENTED_EDGE('',*,*,#8326,.T.);
#11171=ORIENTED_EDGE('',*,*,#8323,.T.);
#11172=ORIENTED_EDGE('',*,*,#8326,.F.);
#11173=ORIENTED_EDGE('',*,*,#8325,.T.);
#11174=ORIENTED_EDGE('',*,*,#8327,.F.);
#11175=ORIENTED_EDGE('',*,*,#8328,.F.);
#11176=ORIENTED_EDGE('',*,*,#8329,.T.);
#11177=ORIENTED_EDGE('',*,*,#8327,.T.);
#11178=ORIENTED_EDGE('',*,*,#8329,.F.);
#11179=ORIENTED_EDGE('',*,*,#8319,.T.);
#11180=ORIENTED_EDGE('',*,*,#8330,.T.);
#11181=ORIENTED_EDGE('',*,*,#8328,.T.);
#11182=ORIENTED_EDGE('',*,*,#8330,.F.);
#11601=CYLINDRICAL_SURFACE('',#15384,0.35);
#11602=CYLINDRICAL_SURFACE('',#15392,0.1954);
#12350=ADVANCED_FACE('',(#2625),#1865,.F.);
#12351=ADVANCED_FACE('',(#2626),#1866,.F.);
#12352=ADVANCED_FACE('',(#2627),#1867,.F.);
#12353=ADVANCED_FACE('',(#2628),#1868,.F.);
#12354=ADVANCED_FACE('',(#2629),#1869,.F.);
#12355=ADVANCED_FACE('',(#2630),#1870,.F.);
#12356=ADVANCED_FACE('',(#2631),#1871,.F.);
#12357=ADVANCED_FACE('',(#2632),#1872,.F.);
#12358=ADVANCED_FACE('',(#2633),#1873,.F.);
#12359=ADVANCED_FACE('',(#2634),#1874,.T.);
#12360=ADVANCED_FACE('',(#2635),#644,.T.);
#12361=ADVANCED_FACE('',(#2636),#11601,.T.);
#12362=ADVANCED_FACE('',(#2637),#645,.T.);
#12363=ADVANCED_FACE('',(#2638,#1481),#1875,.T.);
#12364=ADVANCED_FACE('',(#2639),#646,.T.);
#12365=ADVANCED_FACE('',(#2640),#11602,.T.);
#12501=CLOSED_SHELL('',(#12350,#12351,#12352,#12353,#12354,#12355,#12356,
#12357));
#12502=CLOSED_SHELL('',(#12358,#12359,#12360,#12361,#12362,#12363,#12364,
#12365));
#15369=AXIS2_PLACEMENT_3D('',#23302,#19494,#19495);
#15370=AXIS2_PLACEMENT_3D('',#23303,#19496,#19497);
#15371=AXIS2_PLACEMENT_3D('',#23312,#19502,#19503);
#15372=AXIS2_PLACEMENT_3D('',#23318,#19507,#19508);
#15373=AXIS2_PLACEMENT_3D('',#23324,#19512,#19513);
#15374=AXIS2_PLACEMENT_3D('',#23330,#19517,#19518);
#15375=AXIS2_PLACEMENT_3D('',#23336,#19522,#19523);
#15376=AXIS2_PLACEMENT_3D('',#23339,#19526,#19527);
#15377=AXIS2_PLACEMENT_3D('',#23340,#19528,#19529);
#15378=AXIS2_PLACEMENT_3D('',#23341,#19530,#19531);
#15379=AXIS2_PLACEMENT_3D('',#23343,#19532,#19533);
#15380=AXIS2_PLACEMENT_3D('',#23344,#19534,#19535);
#15381=AXIS2_PLACEMENT_3D('',#23346,#19536,#19537);
#15382=AXIS2_PLACEMENT_3D('',#23347,#19538,#19539);
#15383=AXIS2_PLACEMENT_3D('',#23349,#19540,#19541);
#15384=AXIS2_PLACEMENT_3D('',#23351,#19543,#19544);
#15385=AXIS2_PLACEMENT_3D('',#23353,#19545,#19546);
#15386=AXIS2_PLACEMENT_3D('',#23355,#19548,#19549);
#15387=AXIS2_PLACEMENT_3D('',#23357,#19550,#19551);
#15388=AXIS2_PLACEMENT_3D('',#23359,#19553,#19554);
#15389=AXIS2_PLACEMENT_3D('',#23361,#19555,#19556);
#15390=AXIS2_PLACEMENT_3D('',#23362,#19557,#19558);
#15391=AXIS2_PLACEMENT_3D('',#23364,#19559,#19560);
#15392=AXIS2_PLACEMENT_3D('',#23366,#19562,#19563);
#19494=DIRECTION('axis',(0.,0.,1.));
#19495=DIRECTION('refdir',(1.,0.,0.));
#19496=DIRECTION('center_axis',(0.866025403784439,0.,-0.5));
#19497=DIRECTION('ref_axis',(0.5,0.,0.866025403784439));
#19498=DIRECTION('',(-0.5,0.,-0.866025403784439));
#19499=DIRECTION('',(0.,-1.,0.));
#19500=DIRECTION('',(0.5,0.,0.866025403784439));
#19501=DIRECTION('',(0.,-1.,0.));
#19502=DIRECTION('center_axis',(1.60246890531964E-16,0.,-1.));
#19503=DIRECTION('ref_axis',(1.,0.,1.60246890531964E-16));
#19504=DIRECTION('',(-1.,0.,-1.60246890531964E-16));
#19505=DIRECTION('',(0.,-1.,0.));
#19506=DIRECTION('',(1.,0.,1.60246890531964E-16));
#19507=DIRECTION('center_axis',(-0.866025403784439,0.,-0.5));
#19508=DIRECTION('ref_axis',(0.5,0.,-0.866025403784439));
#19509=DIRECTION('',(-0.5,0.,0.866025403784439));
#19510=DIRECTION('',(0.,-1.,0.));
#19511=DIRECTION('',(0.5,0.,-0.866025403784439));
#19512=DIRECTION('center_axis',(-0.866025403784439,0.,0.5));
#19513=DIRECTION('ref_axis',(-0.5,0.,-0.866025403784439));
#19514=DIRECTION('',(0.5,0.,0.866025403784439));
#19515=DIRECTION('',(0.,-1.,0.));
#19516=DIRECTION('',(-0.5,0.,-0.866025403784439));
#19517=DIRECTION('center_axis',(-1.60246890531964E-16,0.,1.));
#19518=DIRECTION('ref_axis',(-1.,0.,-1.60246890531964E-16));
#19519=DIRECTION('',(1.,0.,1.60246890531964E-16));
#19520=DIRECTION('',(0.,-1.,0.));
#19521=DIRECTION('',(-1.,0.,-1.60246890531964E-16));
#19522=DIRECTION('center_axis',(0.866025403784439,0.,0.5));
#19523=DIRECTION('ref_axis',(-0.5,0.,0.866025403784439));
#19524=DIRECTION('',(0.5,0.,-0.866025403784439));
#19525=DIRECTION('',(-0.5,0.,0.866025403784439));
#19526=DIRECTION('center_axis',(0.,1.,0.));
#19527=DIRECTION('ref_axis',(1.,0.,0.));
#19528=DIRECTION('center_axis',(0.,-1.,0.));
#19529=DIRECTION('ref_axis',(0.,0.,-1.));
#19530=DIRECTION('center_axis',(0.,1.,0.));
#19531=DIRECTION('ref_axis',(1.,0.,0.));
#19532=DIRECTION('center_axis',(0.,1.,0.));
#19533=DIRECTION('ref_axis',(1.,0.,0.));
#19534=DIRECTION('center_axis',(0.,1.,0.));
#19535=DIRECTION('ref_axis',(0.,0.,1.));
#19536=DIRECTION('center_axis',(0.,-1.,0.));
#19537=DIRECTION('ref_axis',(1.,0.,0.));
#19538=DIRECTION('center_axis',(0.,-1.,0.));
#19539=DIRECTION('ref_axis',(1.,0.,0.));
#19540=DIRECTION('center_axis',(0.,-1.,0.));
#19541=DIRECTION('ref_axis',(1.,0.,0.));
#19542=DIRECTION('',(0.707106781186547,0.707106781186548,8.65956056235493E-17));
#19543=DIRECTION('center_axis',(0.,-1.,0.));
#19544=DIRECTION('ref_axis',(1.,0.,0.));
#19545=DIRECTION('center_axis',(0.,-1.,0.));
#19546=DIRECTION('ref_axis',(1.,0.,0.));
#19547=DIRECTION('',(0.,1.,0.));
#19548=DIRECTION('center_axis',(0.,1.,0.));
#19549=DIRECTION('ref_axis',(1.,0.,0.));
#19550=DIRECTION('center_axis',(0.,-1.,0.));
#19551=DIRECTION('ref_axis',(1.,0.,0.));
#19552=DIRECTION('',(-0.707106781186547,0.707106781186548,-8.65956056235493E-17));
#19553=DIRECTION('center_axis',(0.,-1.,0.));
#19554=DIRECTION('ref_axis',(0.,0.,-1.));
#19555=DIRECTION('center_axis',(0.,-1.,0.));
#19556=DIRECTION('ref_axis',(1.,0.,0.));
#19557=DIRECTION('center_axis',(0.,1.,0.));
#19558=DIRECTION('ref_axis',(1.,0.,0.));
#19559=DIRECTION('center_axis',(0.,1.,0.));
#19560=DIRECTION('ref_axis',(1.,0.,0.));
#19561=DIRECTION('',(-0.447213595499958,0.894427190999916,-5.47678698264203E-17));
#19562=DIRECTION('center_axis',(0.,-1.,0.));
#19563=DIRECTION('ref_axis',(1.,0.,0.));
#19564=DIRECTION('',(0.,1.,0.));
#23302=CARTESIAN_POINT('',(0.,0.,0.));
#23303=CARTESIAN_POINT('Origin',(0.0866025403784439,-0.4,-0.15));
#23304=CARTESIAN_POINT('',(0.173205080756888,-0.4,0.));
#23305=CARTESIAN_POINT('',(0.0866025403784439,-0.4,-0.15));
#23306=CARTESIAN_POINT('',(0.173205080756888,-0.4,0.));
#23307=CARTESIAN_POINT('',(0.0866025403784439,-0.64,-0.15));
#23308=CARTESIAN_POINT('',(0.0866025403784439,-0.4,-0.15));
#23309=CARTESIAN_POINT('',(0.173205080756888,-0.64,0.));
#23310=CARTESIAN_POINT('',(0.173205080756888,-0.64,0.));
#23311=CARTESIAN_POINT('',(0.173205080756888,-0.4,0.));
#23312=CARTESIAN_POINT('Origin',(-0.0866025403784438,-0.4,-0.15));
#23313=CARTESIAN_POINT('',(-0.0866025403784438,-0.4,-0.15));
#23314=CARTESIAN_POINT('',(0.0866025403784439,-0.4,-0.15));
#23315=CARTESIAN_POINT('',(-0.0866025403784438,-0.64,-0.15));
#23316=CARTESIAN_POINT('',(-0.0866025403784438,-0.4,-0.15));
#23317=CARTESIAN_POINT('',(0.0866025403784439,-0.64,-0.15));
#23318=CARTESIAN_POINT('Origin',(-0.173205080756888,-0.4,-2.77555756156289E-17));
#23319=CARTESIAN_POINT('',(-0.173205080756888,-0.4,-2.12115047744981E-17));
#23320=CARTESIAN_POINT('',(-0.0866025403784438,-0.4,-0.15));
#23321=CARTESIAN_POINT('',(-0.173205080756888,-0.64,-2.77555756156289E-17));
#23322=CARTESIAN_POINT('',(-0.173205080756888,-0.4,-2.12115047744981E-17));
#23323=CARTESIAN_POINT('',(-0.0866025403784438,-0.64,-0.15));
#23324=CARTESIAN_POINT('Origin',(-0.0866025403784439,-0.4,0.15));
#23325=CARTESIAN_POINT('',(-0.0866025403784439,-0.4,0.15));
#23326=CARTESIAN_POINT('',(-0.173205080756888,-0.4,-2.12115047744981E-17));
#23327=CARTESIAN_POINT('',(-0.0866025403784439,-0.64,0.15));
#23328=CARTESIAN_POINT('',(-0.0866025403784439,-0.4,0.15));
#23329=CARTESIAN_POINT('',(-0.173205080756888,-0.64,-2.12115047744981E-17));
#23330=CARTESIAN_POINT('Origin',(0.0866025403784439,-0.4,0.15));
#23331=CARTESIAN_POINT('',(0.0866025403784439,-0.4,0.15));
#23332=CARTESIAN_POINT('',(-0.0866025403784439,-0.4,0.15));
#23333=CARTESIAN_POINT('',(0.0866025403784439,-0.64,0.15));
#23334=CARTESIAN_POINT('',(0.0866025403784439,-0.4,0.15));
#23335=CARTESIAN_POINT('',(-0.0866025403784439,-0.64,0.15));
#23336=CARTESIAN_POINT('Origin',(0.173205080756888,-0.4,0.));
#23337=CARTESIAN_POINT('',(0.0866025403784439,-0.4,0.15));
#23338=CARTESIAN_POINT('',(0.0866025403784439,-0.64,0.15));
#23339=CARTESIAN_POINT('Origin',(0.,-0.4,-2.77555756156289E-17));
#23340=CARTESIAN_POINT('Origin',(0.,-0.64,-2.77555756156289E-17));
#23341=CARTESIAN_POINT('Origin',(0.,-1.,0.));
#23342=CARTESIAN_POINT('',(-0.1954,-1.,2.39295984553393E-17));
#23343=CARTESIAN_POINT('Origin',(0.,-1.,0.));
#23344=CARTESIAN_POINT('Origin',(0.3,0.4,0.));
#23345=CARTESIAN_POINT('',(-0.3,0.4,-3.67394039744206E-17));
#23346=CARTESIAN_POINT('Origin',(0.,0.4,0.));
#23347=CARTESIAN_POINT('Origin',(0.,0.375,0.));
#23348=CARTESIAN_POINT('',(-0.35,0.35,-4.28626379701573E-17));
#23349=CARTESIAN_POINT('Origin',(0.,0.35,0.));
#23350=CARTESIAN_POINT('',(-0.325,0.375,-3.9801020972289E-17));
#23351=CARTESIAN_POINT('Origin',(0.,0.19,0.));
#23352=CARTESIAN_POINT('',(-0.35,0.03,-4.28626379701574E-17));
#23353=CARTESIAN_POINT('Origin',(0.,0.03,0.));
#23354=CARTESIAN_POINT('',(-0.35,0.19,-4.28626379701574E-17));
#23355=CARTESIAN_POINT('Origin',(0.,0.0149999999999999,0.));
#23356=CARTESIAN_POINT('',(-0.32,-3.29597460435593E-17,-3.91886975727153E-17));
#23357=CARTESIAN_POINT('Origin',(0.,0.,0.));
#23358=CARTESIAN_POINT('',(-0.335,0.0149999999999999,-4.10256677714363E-17));
#23359=CARTESIAN_POINT('Origin',(0.22,0.,0.));
#23360=CARTESIAN_POINT('',(-0.22,-6.93889390390723E-18,-2.69422295812418E-17));
#23361=CARTESIAN_POINT('Origin',(0.,0.,0.));
#23362=CARTESIAN_POINT('Origin',(0.,-0.02,0.));
#23363=CARTESIAN_POINT('',(-0.1954,-0.0492,2.39295984553393E-17));
#23364=CARTESIAN_POINT('Origin',(0.,-0.0492,0.));
#23365=CARTESIAN_POINT('',(-0.21,-0.02,-2.57175827820944E-17));
#23366=CARTESIAN_POINT('Origin',(0.,-0.8,0.));
#23367=CARTESIAN_POINT('',(-0.1954,-0.8,-2.39295984553393E-17));
#23602=UNCERTAINTY_MEASURE_WITH_UNIT(LENGTH_MEASURE(0.001),#23729,
'DISTANCE_ACCURACY_VALUE',
'Maximum model space distance between geometric entities at asserted c
onnectivities');
#23611=UNCERTAINTY_MEASURE_WITH_UNIT(LENGTH_MEASURE(0.001),#23729,
'DISTANCE_ACCURACY_VALUE',
'Maximum model space distance between geometric entities at asserted c
onnectivities');
#23719=(
GEOMETRIC_REPRESENTATION_CONTEXT(3)
GLOBAL_UNCERTAINTY_ASSIGNED_CONTEXT((#23602))
GLOBAL_UNIT_ASSIGNED_CONTEXT((#23729,#23731,#23732))
REPRESENTATION_CONTEXT('','3D')
);
#23728=(
GEOMETRIC_REPRESENTATION_CONTEXT(3)
GLOBAL_UNCERTAINTY_ASSIGNED_CONTEXT((#23611))
GLOBAL_UNIT_ASSIGNED_CONTEXT((#23729,#23731,#23732))
REPRESENTATION_CONTEXT('','3D')
);
#23729=(
LENGTH_UNIT()
NAMED_UNIT(*)
SI_UNIT(.CENTI.,.METRE.)
);
#23731=(
NAMED_UNIT(*)
PLANE_ANGLE_UNIT()
SI_UNIT($,.RADIAN.)
);
#23732=(
NAMED_UNIT(*)
SI_UNIT($,.STERADIAN.)
SOLID_ANGLE_UNIT()
);
#23840=SHAPE_DEFINITION_REPRESENTATION(#24080,#24219);
#24080=PRODUCT_DEFINITION_SHAPE('',$,#24336);
#24219=SHAPE_REPRESENTATION('',(#15369),#23719);
#24228=PRODUCT_DEFINITION_CONTEXT('part definition',#24578,'design');
#24336=PRODUCT_DEFINITION('M4x10 Cap Screw','M4x10 Cap Screw',#24452,#24228);
#24452=PRODUCT_DEFINITION_FORMATION('',$,#24687);
#24578=APPLICATION_CONTEXT(
'Core Data for Automotive Mechanical Design Process');
#24579=PRODUCT_CONTEXT('part definition',#24578,'mechanical');
#24687=PRODUCT('M4x10 Cap Screw','M4x10 Cap Screw','M4x10 Cap Screw',(#24579));
#24766=COLOUR_RGB('Black',0.12,0.14,0.17);
#24767=FILL_AREA_STYLE_COLOUR('',#24766);
#24768=FILL_AREA_STYLE('',(#24767));
#24769=SURFACE_STYLE_FILL_AREA(#24768);
#24770=SURFACE_SIDE_STYLE('',(#24769));
#24771=SURFACE_STYLE_USAGE(.BOTH.,#24770);
#24772=PRESENTATION_STYLE_ASSIGNMENT((#24771));
ENDSEC;
END-ISO-10303-21;
